ISO-10303-21;
HEADER;
/* Generated by software containing ST-Developer
 * from STEP Tools, Inc. (www.steptools.com) 
 */

FILE_DESCRIPTION(
/* description */ ('Shaft runout checking stand'),
/* implementation_level */ '2;1');

FILE_NAME(
/* name */ 'Bonded outer race retainer (1).step',
/* time_stamp */ '2026-11-02T21:12:33-08:00',
/* author */ (''),
/* organization */ (''),
/* preprocessor_version */ 'ST-DEVELOPER v20.2',
/* originating_system */ 'Autodesk Translation Framework v15.17.0.0',
/* authorisation */ '');

FILE_SCHEMA (('AUTOMOTIVE_DESIGN { 1 0 10303 214 3 1 1 }'));
ENDSEC;

DATA;
#10=MECHANICAL_DESIGN_GEOMETRIC_PRESENTATION_REPRESENTATION('',(#513),#11748);
#419=SHAPE_REPRESENTATION_RELATIONSHIP('SRR','None',#11971,#462);
#462=ADVANCED_BREP_SHAPE_REPRESENTATION('',(#561),#11747);
#513=STYLED_ITEM('',(#12169),#561);
#561=MANIFOLD_SOLID_BREP('Body1',#6259);
#671=FACE_BOUND('',#1882,.T.);
#672=FACE_BOUND('',#1884,.T.);
#934=CIRCLE('',#7475,1.1);
#935=CIRCLE('',#7476,1.1);
#936=CIRCLE('',#7478,1.8);
#937=CIRCLE('',#7479,1.8);
#1036=CYLINDRICAL_SURFACE('',#7474,1.1);
#1037=CYLINDRICAL_SURFACE('',#7477,1.8);
#1402=FACE_OUTER_BOUND('',#1879,.T.);
#1403=FACE_OUTER_BOUND('',#1880,.T.);
#1404=FACE_OUTER_BOUND('',#1881,.T.);
#1405=FACE_OUTER_BOUND('',#1883,.T.);
#1879=EDGE_LOOP('',(#5592,#5593,#5594,#5595));
#1880=EDGE_LOOP('',(#5596,#5597,#5598,#5599));
#1881=EDGE_LOOP('',(#5600));
#1882=EDGE_LOOP('',(#5601));
#1883=EDGE_LOOP('',(#5602));
#1884=EDGE_LOOP('',(#5603));
#2350=LINE('',#11631,#2817);
#2351=LINE('',#11637,#2818);
#2817=VECTOR('',#9441,1.1);
#2818=VECTOR('',#9448,1.8);
#3326=VERTEX_POINT('',#11628);
#3327=VERTEX_POINT('',#11630);
#3328=VERTEX_POINT('',#11634);
#3329=VERTEX_POINT('',#11636);
#4082=EDGE_CURVE('',#3326,#3326,#934,.T.);
#4083=EDGE_CURVE('',#3326,#3327,#2350,.T.);
#4084=EDGE_CURVE('',#3327,#3327,#935,.T.);
#4085=EDGE_CURVE('',#3328,#3328,#936,.T.);
#4086=EDGE_CURVE('',#3328,#3329,#2351,.T.);
#4087=EDGE_CURVE('',#3329,#3329,#937,.T.);
#5592=ORIENTED_EDGE('',*,*,#4082,.F.);
#5593=ORIENTED_EDGE('',*,*,#4083,.T.);
#5594=ORIENTED_EDGE('',*,*,#4084,.T.);
#5595=ORIENTED_EDGE('',*,*,#4083,.F.);
#5596=ORIENTED_EDGE('',*,*,#4085,.F.);
#5597=ORIENTED_EDGE('',*,*,#4086,.T.);
#5598=ORIENTED_EDGE('',*,*,#4087,.T.);
#5599=ORIENTED_EDGE('',*,*,#4086,.F.);
#5600=ORIENTED_EDGE('',*,*,#4085,.T.);
#5601=ORIENTED_EDGE('',*,*,#4082,.T.);
#5602=ORIENTED_EDGE('',*,*,#4087,.F.);
#5603=ORIENTED_EDGE('',*,*,#4084,.F.);
#5836=PLANE('',#7480);
#5837=PLANE('',#7481);
#6202=ADVANCED_FACE('',(#1402),#1036,.F.);
#6203=ADVANCED_FACE('',(#1403),#1037,.T.);
#6204=ADVANCED_FACE('',(#1404,#671),#5836,.T.);
#6205=ADVANCED_FACE('',(#1405,#672),#5837,.F.);
#6259=CLOSED_SHELL('',(#6202,#6203,#6204,#6205));
#7473=AXIS2_PLACEMENT_3D('',#11626,#9435,#9436);
#7474=AXIS2_PLACEMENT_3D('',#11627,#9437,#9438);
#7475=AXIS2_PLACEMENT_3D('',#11629,#9439,#9440);
#7476=AXIS2_PLACEMENT_3D('',#11632,#9442,#9443);
#7477=AXIS2_PLACEMENT_3D('',#11633,#9444,#9445);
#7478=AXIS2_PLACEMENT_3D('',#11635,#9446,#9447);
#7479=AXIS2_PLACEMENT_3D('',#11638,#9449,#9450);
#7480=AXIS2_PLACEMENT_3D('',#11639,#9451,#9452);
#7481=AXIS2_PLACEMENT_3D('',#11640,#9453,#9454);
#9435=DIRECTION('axis',(0.,0.,1.));
#9436=DIRECTION('refdir',(1.,0.,0.));
#9437=DIRECTION('center_axis',(0.,1.,0.));
#9438=DIRECTION('ref_axis',(1.,0.,0.));
#9439=DIRECTION('center_axis',(0.,-1.,0.));
#9440=DIRECTION('ref_axis',(1.,0.,0.));
#9441=DIRECTION('',(0.,-1.,0.));
#9442=DIRECTION('center_axis',(0.,-1.,0.));
#9443=DIRECTION('ref_axis',(1.,0.,0.));
#9444=DIRECTION('center_axis',(0.,1.,0.));
#9445=DIRECTION('ref_axis',(1.,0.,0.));
#9446=DIRECTION('center_axis',(0.,1.,0.));
#9447=DIRECTION('ref_axis',(1.,0.,0.));
#9448=DIRECTION('',(0.,-1.,0.));
#9449=DIRECTION('center_axis',(0.,1.,0.));
#9450=DIRECTION('ref_axis',(1.,0.,0.));
#9451=DIRECTION('center_axis',(0.,1.,0.));
#9452=DIRECTION('ref_axis',(1.,0.,0.));
#9453=DIRECTION('center_axis',(0.,1.,0.));
#9454=DIRECTION('ref_axis',(1.,0.,0.));
#11626=CARTESIAN_POINT('',(0.,0.,0.));
#11627=CARTESIAN_POINT('Origin',(-2.,-9.55,5.));
#11628=CARTESIAN_POINT('',(-3.1,-9.35,5.));
#11629=CARTESIAN_POINT('Origin',(-2.,-9.35,5.));
#11630=CARTESIAN_POINT('',(-3.1,-9.55,5.));
#11631=CARTESIAN_POINT('',(-3.1,-9.55,5.));
#11632=CARTESIAN_POINT('Origin',(-2.,-9.55,5.));
#11633=CARTESIAN_POINT('Origin',(-2.,-9.55,5.));
#11634=CARTESIAN_POINT('',(-3.8,-9.35,5.));
#11635=CARTESIAN_POINT('Origin',(-2.,-9.35,5.));
#11636=CARTESIAN_POINT('',(-3.8,-9.55,5.));
#11637=CARTESIAN_POINT('',(-3.8,-9.55,5.));
#11638=CARTESIAN_POINT('Origin',(-2.,-9.55,5.));
#11639=CARTESIAN_POINT('Origin',(-2.,-9.35,5.));
#11640=CARTESIAN_POINT('Origin',(-2.,-9.55,5.));
#11698=UNCERTAINTY_MEASURE_WITH_UNIT(LENGTH_MEASURE(0.001),#11749,
'DISTANCE_ACCURACY_VALUE',
'Maximum model space distance between geometric entities at asserted c
onnectivities');
#11699=UNCERTAINTY_MEASURE_WITH_UNIT(LENGTH_MEASURE(0.001),#11749,
'DISTANCE_ACCURACY_VALUE',
'Maximum model space distance between geometric entities at asserted c
onnectivities');
#11747=(
GEOMETRIC_REPRESENTATION_CONTEXT(3)
GLOBAL_UNCERTAINTY_ASSIGNED_CONTEXT((#11698))
GLOBAL_UNIT_ASSIGNED_CONTEXT((#11749,#11751,#11752))
REPRESENTATION_CONTEXT('','3D')
);
#11748=(
GEOMETRIC_REPRESENTATION_CONTEXT(3)
GLOBAL_UNCERTAINTY_ASSIGNED_CONTEXT((#11699))
GLOBAL_UNIT_ASSIGNED_CONTEXT((#11749,#11751,#11752))
REPRESENTATION_CONTEXT('','3D')
);
#11749=(
LENGTH_UNIT()
NAMED_UNIT(*)
SI_UNIT(.CENTI.,.METRE.)
);
#11751=(
NAMED_UNIT(*)
PLANE_ANGLE_UNIT()
SI_UNIT($,.RADIAN.)
);
#11752=(
NAMED_UNIT(*)
SI_UNIT($,.STERADIAN.)
SOLID_ANGLE_UNIT()
);
#11800=SHAPE_DEFINITION_REPRESENTATION(#11913,#11971);
#11913=PRODUCT_DEFINITION_SHAPE('',$,#12020);
#11971=SHAPE_REPRESENTATION('',(#7473),#11747);
#11972=PRODUCT_DEFINITION_CONTEXT('part definition',#12118,'design');
#12020=PRODUCT_DEFINITION('Bonded outer race retainer_1',
'Bonded outer race retainer (1)',#12068,#11972);
#12068=PRODUCT_DEFINITION_FORMATION('',$,#12167);
#12118=APPLICATION_CONTEXT(
'Core Data for Automotive Mechanical Design Process');
#12119=PRODUCT_CONTEXT('part definition',#12118,'mechanical');
#12167=PRODUCT('Bonded outer race retainer_1',
'Bonded outer race retainer (1)','Bonded outer race retainer',(#12119));
#12169=PRESENTATION_STYLE_ASSIGNMENT((#12174));
#12174=SURFACE_STYLE_USAGE(.BOTH.,#12179);
#12179=SURFACE_SIDE_STYLE('',(#12184));
#12184=SURFACE_STYLE_FILL_AREA(#12189);
#12189=FILL_AREA_STYLE('CAD Library Painted - Engineering blue',(#12194));
#12194=FILL_AREA_STYLE_COLOUR('CAD Library Painted - Engineering blue',
#12199);
#12199=COLOUR_RGB('CAD Library Painted - Engineering blue',0.12156862745098,
0.356862745098039,0.6);
ENDSEC;
END-ISO-10303-21;
